ISO-10303-21;
HEADER;
/* Generated by software containing ST-Developer
 * from STEP Tools, Inc. (www.steptools.com) 
 */

FILE_DESCRIPTION(
/* description */ ('V-block with clamp strap'),
/* implementation_level */ '2;1');

FILE_NAME(
/* name */ 'Cap Screw - M6x25.step',
/* time_stamp */ '2026-10-27T10:50:53-07:00',
/* author */ (''),
/* organization */ (''),
/* preprocessor_version */ 'ST-DEVELOPER v20.2',
/* originating_system */ 'Autodesk Translation Framework v15.17.0.0',
/* authorisation */ '');

FILE_SCHEMA (('AUTOMOTIVE_DESIGN { 1 0 10303 214 3 1 1 }'));
ENDSEC;

DATA;
#10=MECHANICAL_DESIGN_GEOMETRIC_PRESENTATION_REPRESENTATION('',(#275),#7344);
#199=ORIENTED_CLOSED_SHELL('',*,#4158,.F.);
#202=CONICAL_SURFACE('',#4623,0.475,0.785398163397449);
#203=CONICAL_SURFACE('',#4627,0.485,0.785398163397448);
#204=CONICAL_SURFACE('',#4631,0.31,0.463647609000806);
#205=CONICAL_SURFACE('',#4635,0.27,0.785398163397448);
#217=BREP_WITH_VOIDS('Body1',#4157,(#199));
#233=SHAPE_REPRESENTATION_RELATIONSHIP('SRR','None',#7451,#254);
#254=ADVANCED_BREP_SHAPE_REPRESENTATION('',(#217),#7330);
#275=STYLED_ITEM('',(#7638),#217);
#355=FACE_BOUND('',#988,.T.);
#446=CIRCLE('',#4622,0.45);
#447=CIRCLE('',#4624,0.5);
#448=CIRCLE('',#4626,0.5);
#449=CIRCLE('',#4628,0.47);
#450=CIRCLE('',#4630,0.32);
#451=CIRCLE('',#4632,0.2942);
#452=CIRCLE('',#4634,0.2942);
#453=CIRCLE('',#4636,0.24);
#540=CYLINDRICAL_SURFACE('',#4625,0.5);
#541=CYLINDRICAL_SURFACE('',#4633,0.2942);
#693=FACE_OUTER_BOUND('',#983,.T.);
#694=FACE_OUTER_BOUND('',#984,.T.);
#695=FACE_OUTER_BOUND('',#985,.T.);
#696=FACE_OUTER_BOUND('',#986,.T.);
#697=FACE_OUTER_BOUND('',#987,.T.);
#698=FACE_OUTER_BOUND('',#989,.T.);
#699=FACE_OUTER_BOUND('',#990,.T.);
#700=FACE_OUTER_BOUND('',#991,.T.);
#701=FACE_OUTER_BOUND('',#992,.T.);
#702=FACE_OUTER_BOUND('',#993,.T.);
#703=FACE_OUTER_BOUND('',#994,.T.);
#704=FACE_OUTER_BOUND('',#995,.T.);
#705=FACE_OUTER_BOUND('',#996,.T.);
#706=FACE_OUTER_BOUND('',#997,.T.);
#707=FACE_OUTER_BOUND('',#998,.T.);
#708=FACE_OUTER_BOUND('',#999,.T.);
#709=FACE_OUTER_BOUND('',#1000,.T.);
#983=EDGE_LOOP('',(#3326));
#984=EDGE_LOOP('',(#3327,#3328,#3329,#3330));
#985=EDGE_LOOP('',(#3331,#3332,#3333,#3334));
#986=EDGE_LOOP('',(#3335,#3336,#3337,#3338));
#987=EDGE_LOOP('',(#3339));
#988=EDGE_LOOP('',(#3340));
#989=EDGE_LOOP('',(#3341,#3342,#3343,#3344));
#990=EDGE_LOOP('',(#3345,#3346,#3347,#3348));
#991=EDGE_LOOP('',(#3349,#3350,#3351,#3352));
#992=EDGE_LOOP('',(#3353));
#993=EDGE_LOOP('',(#3354,#3355,#3356,#3357));
#994=EDGE_LOOP('',(#3358,#3359,#3360,#3361));
#995=EDGE_LOOP('',(#3362,#3363,#3364,#3365));
#996=EDGE_LOOP('',(#3366,#3367,#3368,#3369));
#997=EDGE_LOOP('',(#3370,#3371,#3372,#3373));
#998=EDGE_LOOP('',(#3374,#3375,#3376,#3377));
#999=EDGE_LOOP('',(#3378,#3379,#3380,#3381,#3382,#3383));
#1000=EDGE_LOOP('',(#3384,#3385,#3386,#3387,#3388,#3389));
#1354=LINE('',#6748,#1719);
#1355=LINE('',#6752,#1720);
#1356=LINE('',#6756,#1721);
#1357=LINE('',#6763,#1722);
#1358=LINE('',#6767,#1723);
#1359=LINE('',#6771,#1724);
#1360=LINE('',#6776,#1725);
#1361=LINE('',#6778,#1726);
#1362=LINE('',#6780,#1727);
#1363=LINE('',#6781,#1728);
#1364=LINE('',#6784,#1729);
#1365=LINE('',#6786,#1730);
#1366=LINE('',#6787,#1731);
#1367=LINE('',#6790,#1732);
#1368=LINE('',#6792,#1733);
#1369=LINE('',#6793,#1734);
#1370=LINE('',#6796,#1735);
#1371=LINE('',#6798,#1736);
#1372=LINE('',#6799,#1737);
#1373=LINE('',#6802,#1738);
#1374=LINE('',#6804,#1739);
#1375=LINE('',#6805,#1740);
#1376=LINE('',#6807,#1741);
#1377=LINE('',#6808,#1742);
#1719=VECTOR('',#5526,0.475);
#1720=VECTOR('',#5531,0.5);
#1721=VECTOR('',#5536,0.485);
#1722=VECTOR('',#5545,0.31);
#1723=VECTOR('',#5550,0.3);
#1724=VECTOR('',#5555,0.27);
#1725=VECTOR('',#5560,1.);
#1726=VECTOR('',#5561,1.);
#1727=VECTOR('',#5562,1.);
#1728=VECTOR('',#5563,1.);
#1729=VECTOR('',#5566,1.);
#1730=VECTOR('',#5567,1.);
#1731=VECTOR('',#5568,1.);
#1732=VECTOR('',#5571,1.);
#1733=VECTOR('',#5572,1.);
#1734=VECTOR('',#5573,1.);
#1735=VECTOR('',#5576,1.);
#1736=VECTOR('',#5577,1.);
#1737=VECTOR('',#5578,1.);
#1738=VECTOR('',#5581,1.);
#1739=VECTOR('',#5582,1.);
#1740=VECTOR('',#5583,1.);
#1741=VECTOR('',#5586,1.);
#1742=VECTOR('',#5587,1.);
#2041=VERTEX_POINT('',#6743);
#2042=VERTEX_POINT('',#6746);
#2043=VERTEX_POINT('',#6750);
#2044=VERTEX_POINT('',#6754);
#2045=VERTEX_POINT('',#6758);
#2046=VERTEX_POINT('',#6761);
#2047=VERTEX_POINT('',#6765);
#2048=VERTEX_POINT('',#6769);
#2049=VERTEX_POINT('',#6774);
#2050=VERTEX_POINT('',#6775);
#2051=VERTEX_POINT('',#6777);
#2052=VERTEX_POINT('',#6779);
#2053=VERTEX_POINT('',#6783);
#2054=VERTEX_POINT('',#6785);
#2055=VERTEX_POINT('',#6789);
#2056=VERTEX_POINT('',#6791);
#2057=VERTEX_POINT('',#6795);
#2058=VERTEX_POINT('',#6797);
#2059=VERTEX_POINT('',#6801);
#2060=VERTEX_POINT('',#6803);
#2489=EDGE_CURVE('',#2041,#2041,#446,.T.);
#2490=EDGE_CURVE('',#2042,#2042,#447,.T.);
#2491=EDGE_CURVE('',#2042,#2041,#1354,.T.);
#2492=EDGE_CURVE('',#2043,#2043,#448,.T.);
#2493=EDGE_CURVE('',#2043,#2042,#1355,.T.);
#2494=EDGE_CURVE('',#2044,#2044,#449,.T.);
#2495=EDGE_CURVE('',#2044,#2043,#1356,.T.);
#2496=EDGE_CURVE('',#2045,#2045,#450,.T.);
#2497=EDGE_CURVE('',#2046,#2046,#451,.F.);
#2498=EDGE_CURVE('',#2046,#2045,#1357,.T.);
#2499=EDGE_CURVE('',#2047,#2047,#452,.F.);
#2500=EDGE_CURVE('',#2047,#2046,#1358,.T.);
#2501=EDGE_CURVE('',#2048,#2048,#453,.T.);
#2502=EDGE_CURVE('',#2048,#2047,#1359,.T.);
#2503=EDGE_CURVE('',#2049,#2050,#1360,.T.);
#2504=EDGE_CURVE('',#2050,#2051,#1361,.T.);
#2505=EDGE_CURVE('',#2051,#2052,#1362,.T.);
#2506=EDGE_CURVE('',#2049,#2052,#1363,.T.);
#2507=EDGE_CURVE('',#2050,#2053,#1364,.T.);
#2508=EDGE_CURVE('',#2053,#2054,#1365,.T.);
#2509=EDGE_CURVE('',#2054,#2051,#1366,.T.);
#2510=EDGE_CURVE('',#2053,#2055,#1367,.T.);
#2511=EDGE_CURVE('',#2055,#2056,#1368,.T.);
#2512=EDGE_CURVE('',#2056,#2054,#1369,.T.);
#2513=EDGE_CURVE('',#2055,#2057,#1370,.T.);
#2514=EDGE_CURVE('',#2057,#2058,#1371,.T.);
#2515=EDGE_CURVE('',#2058,#2056,#1372,.T.);
#2516=EDGE_CURVE('',#2057,#2059,#1373,.T.);
#2517=EDGE_CURVE('',#2059,#2060,#1374,.T.);
#2518=EDGE_CURVE('',#2060,#2058,#1375,.T.);
#2519=EDGE_CURVE('',#2059,#2049,#1376,.T.);
#2520=EDGE_CURVE('',#2052,#2060,#1377,.T.);
#3326=ORIENTED_EDGE('',*,*,#2489,.F.);
#3327=ORIENTED_EDGE('',*,*,#2490,.F.);
#3328=ORIENTED_EDGE('',*,*,#2491,.T.);
#3329=ORIENTED_EDGE('',*,*,#2489,.T.);
#3330=ORIENTED_EDGE('',*,*,#2491,.F.);
#3331=ORIENTED_EDGE('',*,*,#2492,.F.);
#3332=ORIENTED_EDGE('',*,*,#2493,.T.);
#3333=ORIENTED_EDGE('',*,*,#2490,.T.);
#3334=ORIENTED_EDGE('',*,*,#2493,.F.);
#3335=ORIENTED_EDGE('',*,*,#2494,.F.);
#3336=ORIENTED_EDGE('',*,*,#2495,.T.);
#3337=ORIENTED_EDGE('',*,*,#2492,.T.);
#3338=ORIENTED_EDGE('',*,*,#2495,.F.);
#3339=ORIENTED_EDGE('',*,*,#2494,.T.);
#3340=ORIENTED_EDGE('',*,*,#2496,.F.);
#3341=ORIENTED_EDGE('',*,*,#2497,.F.);
#3342=ORIENTED_EDGE('',*,*,#2498,.T.);
#3343=ORIENTED_EDGE('',*,*,#2496,.T.);
#3344=ORIENTED_EDGE('',*,*,#2498,.F.);
#3345=ORIENTED_EDGE('',*,*,#2499,.F.);
#3346=ORIENTED_EDGE('',*,*,#2500,.T.);
#3347=ORIENTED_EDGE('',*,*,#2497,.T.);
#3348=ORIENTED_EDGE('',*,*,#2500,.F.);
#3349=ORIENTED_EDGE('',*,*,#2501,.F.);
#3350=ORIENTED_EDGE('',*,*,#2502,.T.);
#3351=ORIENTED_EDGE('',*,*,#2499,.T.);
#3352=ORIENTED_EDGE('',*,*,#2502,.F.);
#3353=ORIENTED_EDGE('',*,*,#2501,.T.);
#3354=ORIENTED_EDGE('',*,*,#2503,.T.);
#3355=ORIENTED_EDGE('',*,*,#2504,.T.);
#3356=ORIENTED_EDGE('',*,*,#2505,.T.);
#3357=ORIENTED_EDGE('',*,*,#2506,.F.);
#3358=ORIENTED_EDGE('',*,*,#2507,.T.);
#3359=ORIENTED_EDGE('',*,*,#2508,.T.);
#3360=ORIENTED_EDGE('',*,*,#2509,.T.);
#3361=ORIENTED_EDGE('',*,*,#2504,.F.);
#3362=ORIENTED_EDGE('',*,*,#2510,.T.);
#3363=ORIENTED_EDGE('',*,*,#2511,.T.);
#3364=ORIENTED_EDGE('',*,*,#2512,.T.);
#3365=ORIENTED_EDGE('',*,*,#2508,.F.);
#3366=ORIENTED_EDGE('',*,*,#2513,.T.);
#3367=ORIENTED_EDGE('',*,*,#2514,.T.);
#3368=ORIENTED_EDGE('',*,*,#2515,.T.);
#3369=ORIENTED_EDGE('',*,*,#2511,.F.);
#3370=ORIENTED_EDGE('',*,*,#2516,.T.);
#3371=ORIENTED_EDGE('',*,*,#2517,.T.);
#3372=ORIENTED_EDGE('',*,*,#2518,.T.);
#3373=ORIENTED_EDGE('',*,*,#2514,.F.);
#3374=ORIENTED_EDGE('',*,*,#2519,.T.);
#3375=ORIENTED_EDGE('',*,*,#2506,.T.);
#3376=ORIENTED_EDGE('',*,*,#2520,.T.);
#3377=ORIENTED_EDGE('',*,*,#2517,.F.);
#3378=ORIENTED_EDGE('',*,*,#2519,.F.);
#3379=ORIENTED_EDGE('',*,*,#2516,.F.);
#3380=ORIENTED_EDGE('',*,*,#2513,.F.);
#3381=ORIENTED_EDGE('',*,*,#2510,.F.);
#3382=ORIENTED_EDGE('',*,*,#2507,.F.);
#3383=ORIENTED_EDGE('',*,*,#2503,.F.);
#3384=ORIENTED_EDGE('',*,*,#2520,.F.);
#3385=ORIENTED_EDGE('',*,*,#2505,.F.);
#3386=ORIENTED_EDGE('',*,*,#2509,.F.);
#3387=ORIENTED_EDGE('',*,*,#2512,.F.);
#3388=ORIENTED_EDGE('',*,*,#2515,.F.);
#3389=ORIENTED_EDGE('',*,*,#2518,.F.);
#3836=PLANE('',#4621);
#3837=PLANE('',#4629);
#3838=PLANE('',#4637);
#3839=PLANE('',#4638);
#3840=PLANE('',#4639);
#3841=PLANE('',#4640);
#3842=PLANE('',#4641);
#3843=PLANE('',#4642);
#3844=PLANE('',#4643);
#3845=PLANE('',#4644);
#3846=PLANE('',#4645);
#4039=ADVANCED_FACE('',(#693),#3836,.T.);
#4040=ADVANCED_FACE('',(#694),#202,.T.);
#4041=ADVANCED_FACE('',(#695),#540,.T.);
#4042=ADVANCED_FACE('',(#696),#203,.T.);
#4043=ADVANCED_FACE('',(#697,#355),#3837,.T.);
#4044=ADVANCED_FACE('',(#698),#204,.T.);
#4045=ADVANCED_FACE('',(#699),#541,.T.);
#4046=ADVANCED_FACE('',(#700),#205,.T.);
#4047=ADVANCED_FACE('',(#701),#3838,.T.);
#4048=ADVANCED_FACE('',(#702),#3839,.F.);
#4049=ADVANCED_FACE('',(#703),#3840,.F.);
#4050=ADVANCED_FACE('',(#704),#3841,.F.);
#4051=ADVANCED_FACE('',(#705),#3842,.F.);
#4052=ADVANCED_FACE('',(#706),#3843,.F.);
#4053=ADVANCED_FACE('',(#707),#3844,.F.);
#4054=ADVANCED_FACE('',(#708),#3845,.F.);
#4055=ADVANCED_FACE('',(#709),#3846,.F.);
#4157=CLOSED_SHELL('',(#4039,#4040,#4041,#4042,#4043,#4044,#4045,#4046,
#4047));
#4158=CLOSED_SHELL('',(#4048,#4049,#4050,#4051,#4052,#4053,#4054,#4055));
#4620=AXIS2_PLACEMENT_3D('',#6741,#5516,#5517);
#4621=AXIS2_PLACEMENT_3D('',#6742,#5518,#5519);
#4622=AXIS2_PLACEMENT_3D('',#6744,#5520,#5521);
#4623=AXIS2_PLACEMENT_3D('',#6745,#5522,#5523);
#4624=AXIS2_PLACEMENT_3D('',#6747,#5524,#5525);
#4625=AXIS2_PLACEMENT_3D('',#6749,#5527,#5528);
#4626=AXIS2_PLACEMENT_3D('',#6751,#5529,#5530);
#4627=AXIS2_PLACEMENT_3D('',#6753,#5532,#5533);
#4628=AXIS2_PLACEMENT_3D('',#6755,#5534,#5535);
#4629=AXIS2_PLACEMENT_3D('',#6757,#5537,#5538);
#4630=AXIS2_PLACEMENT_3D('',#6759,#5539,#5540);
#4631=AXIS2_PLACEMENT_3D('',#6760,#5541,#5542);
#4632=AXIS2_PLACEMENT_3D('',#6762,#5543,#5544);
#4633=AXIS2_PLACEMENT_3D('',#6764,#5546,#5547);
#4634=AXIS2_PLACEMENT_3D('',#6766,#5548,#5549);
#4635=AXIS2_PLACEMENT_3D('',#6768,#5551,#5552);
#4636=AXIS2_PLACEMENT_3D('',#6770,#5553,#5554);
#4637=AXIS2_PLACEMENT_3D('',#6772,#5556,#5557);
#4638=AXIS2_PLACEMENT_3D('',#6773,#5558,#5559);
#4639=AXIS2_PLACEMENT_3D('',#6782,#5564,#5565);
#4640=AXIS2_PLACEMENT_3D('',#6788,#5569,#5570);
#4641=AXIS2_PLACEMENT_3D('',#6794,#5574,#5575);
#4642=AXIS2_PLACEMENT_3D('',#6800,#5579,#5580);
#4643=AXIS2_PLACEMENT_3D('',#6806,#5584,#5585);
#4644=AXIS2_PLACEMENT_3D('',#6809,#5588,#5589);
#4645=AXIS2_PLACEMENT_3D('',#6810,#5590,#5591);
#5516=DIRECTION('axis',(0.,0.,1.));
#5517=DIRECTION('refdir',(1.,0.,0.));
#5518=DIRECTION('center_axis',(0.,1.,0.));
#5519=DIRECTION('ref_axis',(0.,0.,1.));
#5520=DIRECTION('center_axis',(0.,-1.,0.));
#5521=DIRECTION('ref_axis',(1.,0.,0.));
#5522=DIRECTION('center_axis',(0.,-1.,0.));
#5523=DIRECTION('ref_axis',(1.,0.,0.));
#5524=DIRECTION('center_axis',(0.,-1.,0.));
#5525=DIRECTION('ref_axis',(1.,0.,0.));
#5526=DIRECTION('',(0.707106781186548,0.707106781186547,8.65956056235494E-17));
#5527=DIRECTION('center_axis',(0.,-1.,0.));
#5528=DIRECTION('ref_axis',(1.,0.,0.));
#5529=DIRECTION('center_axis',(0.,-1.,0.));
#5530=DIRECTION('ref_axis',(1.,0.,0.));
#5531=DIRECTION('',(0.,1.,0.));
#5532=DIRECTION('center_axis',(0.,1.,0.));
#5533=DIRECTION('ref_axis',(1.,0.,0.));
#5534=DIRECTION('center_axis',(0.,-1.,0.));
#5535=DIRECTION('ref_axis',(1.,0.,0.));
#5536=DIRECTION('',(-0.707106781186547,0.707106781186548,-8.65956056235493E-17));
#5537=DIRECTION('center_axis',(0.,-1.,0.));
#5538=DIRECTION('ref_axis',(0.,0.,-1.));
#5539=DIRECTION('center_axis',(0.,-1.,0.));
#5540=DIRECTION('ref_axis',(1.,0.,0.));
#5541=DIRECTION('center_axis',(0.,1.,0.));
#5542=DIRECTION('ref_axis',(1.,0.,0.));
#5543=DIRECTION('center_axis',(0.,1.,0.));
#5544=DIRECTION('ref_axis',(1.,0.,0.));
#5545=DIRECTION('',(-0.447213595499958,0.894427190999916,-5.47678698264203E-17));
#5546=DIRECTION('center_axis',(0.,-1.,0.));
#5547=DIRECTION('ref_axis',(1.,0.,0.));
#5548=DIRECTION('center_axis',(0.,1.,0.));
#5549=DIRECTION('ref_axis',(1.,0.,0.));
#5550=DIRECTION('',(0.,1.,0.));
#5551=DIRECTION('center_axis',(0.,1.,0.));
#5552=DIRECTION('ref_axis',(1.,0.,0.));
#5553=DIRECTION('center_axis',(0.,-1.,0.));
#5554=DIRECTION('ref_axis',(1.,0.,0.));
#5555=DIRECTION('',(-0.707106781186547,0.707106781186548,-8.65956056235493E-17));
#5556=DIRECTION('center_axis',(0.,-1.,0.));
#5557=DIRECTION('ref_axis',(0.,0.,-1.));
#5558=DIRECTION('center_axis',(0.866025403784439,0.,-0.5));
#5559=DIRECTION('ref_axis',(0.5,0.,0.866025403784439));
#5560=DIRECTION('',(-0.5,0.,-0.866025403784439));
#5561=DIRECTION('',(0.,-1.,0.));
#5562=DIRECTION('',(0.5,0.,0.866025403784439));
#5563=DIRECTION('',(0.,-1.,0.));
#5564=DIRECTION('center_axis',(1.92296268638356E-16,0.,-1.));
#5565=DIRECTION('ref_axis',(1.,0.,1.92296268638356E-16));
#5566=DIRECTION('',(-1.,0.,-1.92296268638356E-16));
#5567=DIRECTION('',(0.,-1.,0.));
#5568=DIRECTION('',(1.,0.,1.92296268638356E-16));
#5569=DIRECTION('center_axis',(-0.866025403784439,0.,-0.5));
#5570=DIRECTION('ref_axis',(0.5,0.,-0.866025403784439));
#5571=DIRECTION('',(-0.5,0.,0.866025403784438));
#5572=DIRECTION('',(0.,-1.,0.));
#5573=DIRECTION('',(0.5,0.,-0.866025403784438));
#5574=DIRECTION('center_axis',(-0.866025403784439,0.,0.5));
#5575=DIRECTION('ref_axis',(-0.5,0.,-0.866025403784439));
#5576=DIRECTION('',(0.5,0.,0.866025403784439));
#5577=DIRECTION('',(0.,-1.,0.));
#5578=DIRECTION('',(-0.5,0.,-0.866025403784439));
#5579=DIRECTION('center_axis',(-1.92296268638356E-16,0.,1.));
#5580=DIRECTION('ref_axis',(-1.,0.,-1.92296268638356E-16));
#5581=DIRECTION('',(1.,0.,1.92296268638356E-16));
#5582=DIRECTION('',(0.,-1.,0.));
#5583=DIRECTION('',(-1.,0.,-1.92296268638356E-16));
#5584=DIRECTION('center_axis',(0.866025403784439,0.,0.5));
#5585=DIRECTION('ref_axis',(-0.5,0.,0.866025403784439));
#5586=DIRECTION('',(0.5,0.,-0.866025403784439));
#5587=DIRECTION('',(-0.5,0.,0.866025403784439));
#5588=DIRECTION('center_axis',(0.,1.,0.));
#5589=DIRECTION('ref_axis',(1.,0.,0.));
#5590=DIRECTION('center_axis',(0.,-1.,0.));
#5591=DIRECTION('ref_axis',(0.,0.,-1.));
#6741=CARTESIAN_POINT('',(0.,0.,0.));
#6742=CARTESIAN_POINT('Origin',(0.45,0.6,0.));
#6743=CARTESIAN_POINT('',(-0.45,0.6,-5.51091059616309E-17));
#6744=CARTESIAN_POINT('Origin',(0.,0.6,0.));
#6745=CARTESIAN_POINT('Origin',(0.,0.575,0.));
#6746=CARTESIAN_POINT('',(-0.5,0.55,-6.12323399573677E-17));
#6747=CARTESIAN_POINT('Origin',(0.,0.55,0.));
#6748=CARTESIAN_POINT('',(-0.475,0.575,-5.81707229594993E-17));
#6749=CARTESIAN_POINT('Origin',(0.,0.29,0.));
#6750=CARTESIAN_POINT('',(-0.5,0.0299999999999998,-6.12323399573677E-17));
#6751=CARTESIAN_POINT('Origin',(0.,0.0299999999999998,0.));
#6752=CARTESIAN_POINT('',(-0.5,0.29,-6.12323399573677E-17));
#6753=CARTESIAN_POINT('Origin',(0.,0.0150000000000001,0.));
#6754=CARTESIAN_POINT('',(-0.47,7.11236625150491E-17,-5.75583995599256E-17));
#6755=CARTESIAN_POINT('Origin',(0.,0.,0.));
#6756=CARTESIAN_POINT('',(-0.485,0.0150000000000001,-5.93953697586466E-17));
#6757=CARTESIAN_POINT('Origin',(0.32,0.,0.));
#6758=CARTESIAN_POINT('',(-0.32,-6.93889390390723E-18,-3.91886975727153E-17));
#6759=CARTESIAN_POINT('Origin',(0.,0.,0.));
#6760=CARTESIAN_POINT('Origin',(0.,-0.02,0.));
#6761=CARTESIAN_POINT('',(-0.2942,-0.0515999999999999,3.60291088309151E-17));
#6762=CARTESIAN_POINT('Origin',(0.,-0.0515999999999999,0.));
#6763=CARTESIAN_POINT('',(-0.31,-0.02,-3.7964050773568E-17));
#6764=CARTESIAN_POINT('Origin',(0.,-1.24,0.));
#6765=CARTESIAN_POINT('',(-0.2942,-2.4458,3.60291088309151E-17));
#6766=CARTESIAN_POINT('Origin',(0.,-2.4458,0.));
#6767=CARTESIAN_POINT('',(-0.2942,-1.24,-3.60291088309151E-17));
#6768=CARTESIAN_POINT('Origin',(0.,-2.47,0.));
#6769=CARTESIAN_POINT('',(-0.24,-2.5,-2.93915231795365E-17));
#6770=CARTESIAN_POINT('Origin',(0.,-2.5,0.));
#6771=CARTESIAN_POINT('',(-0.27,-2.47,-3.30654635769785E-17));
#6772=CARTESIAN_POINT('Origin',(0.,-2.5,0.));
#6773=CARTESIAN_POINT('Origin',(0.144337567297406,-0.6,-0.25));
#6774=CARTESIAN_POINT('',(0.288675134594813,-0.6,0.));
#6775=CARTESIAN_POINT('',(0.144337567297406,-0.6,-0.25));
#6776=CARTESIAN_POINT('',(0.288675134594813,-0.6,0.));
#6777=CARTESIAN_POINT('',(0.144337567297406,-0.96,-0.25));
#6778=CARTESIAN_POINT('',(0.144337567297406,-0.6,-0.25));
#6779=CARTESIAN_POINT('',(0.288675134594813,-0.96,0.));
#6780=CARTESIAN_POINT('',(0.288675134594813,-0.96,0.));
#6781=CARTESIAN_POINT('',(0.288675134594813,-0.6,0.));
#6782=CARTESIAN_POINT('Origin',(-0.144337567297406,-0.6,-0.25));
#6783=CARTESIAN_POINT('',(-0.144337567297406,-0.6,-0.25));
#6784=CARTESIAN_POINT('',(0.144337567297406,-0.6,-0.25));
#6785=CARTESIAN_POINT('',(-0.144337567297406,-0.96,-0.25));
#6786=CARTESIAN_POINT('',(-0.144337567297406,-0.6,-0.25));
#6787=CARTESIAN_POINT('',(0.144337567297406,-0.96,-0.25));
#6788=CARTESIAN_POINT('Origin',(-0.288675134594813,-0.6,-8.32667268468867E-17));
#6789=CARTESIAN_POINT('',(-0.288675134594813,-0.6,-3.53525079574969E-17));
#6790=CARTESIAN_POINT('',(-0.144337567297406,-0.6,-0.25));
#6791=CARTESIAN_POINT('',(-0.288675134594813,-0.96,-5.55111512312578E-17));
#6792=CARTESIAN_POINT('',(-0.288675134594813,-0.6,-3.53525079574969E-17));
#6793=CARTESIAN_POINT('',(-0.144337567297406,-0.96,-0.25));
#6794=CARTESIAN_POINT('Origin',(-0.144337567297407,-0.6,0.25));
#6795=CARTESIAN_POINT('',(-0.144337567297407,-0.6,0.25));
#6796=CARTESIAN_POINT('',(-0.288675134594813,-0.6,-3.53525079574969E-17));
#6797=CARTESIAN_POINT('',(-0.144337567297407,-0.96,0.25));
#6798=CARTESIAN_POINT('',(-0.144337567297407,-0.6,0.25));
#6799=CARTESIAN_POINT('',(-0.288675134594813,-0.96,-3.53525079574969E-17));
#6800=CARTESIAN_POINT('Origin',(0.144337567297406,-0.6,0.25));
#6801=CARTESIAN_POINT('',(0.144337567297406,-0.6,0.25));
#6802=CARTESIAN_POINT('',(-0.144337567297407,-0.6,0.25));
#6803=CARTESIAN_POINT('',(0.144337567297406,-0.96,0.25));
#6804=CARTESIAN_POINT('',(0.144337567297406,-0.6,0.25));
#6805=CARTESIAN_POINT('',(-0.144337567297407,-0.96,0.25));
#6806=CARTESIAN_POINT('Origin',(0.288675134594813,-0.6,0.));
#6807=CARTESIAN_POINT('',(0.144337567297406,-0.6,0.25));
#6808=CARTESIAN_POINT('',(0.144337567297406,-0.96,0.25));
#6809=CARTESIAN_POINT('Origin',(0.,-0.6,0.));
#6810=CARTESIAN_POINT('Origin',(0.,-0.96,0.));
#7304=UNCERTAINTY_MEASURE_WITH_UNIT(LENGTH_MEASURE(0.001),#7345,
'DISTANCE_ACCURACY_VALUE',
'Maximum model space distance between geometric entities at asserted c
onnectivities');
#7318=UNCERTAINTY_MEASURE_WITH_UNIT(LENGTH_MEASURE(0.001),#7345,
'DISTANCE_ACCURACY_VALUE',
'Maximum model space distance between geometric entities at asserted c
onnectivities');
#7330=(
GEOMETRIC_REPRESENTATION_CONTEXT(3)
GLOBAL_UNCERTAINTY_ASSIGNED_CONTEXT((#7304))
GLOBAL_UNIT_ASSIGNED_CONTEXT((#7345,#7347,#7348))
REPRESENTATION_CONTEXT('','3D')
);
#7344=(
GEOMETRIC_REPRESENTATION_CONTEXT(3)
GLOBAL_UNCERTAINTY_ASSIGNED_CONTEXT((#7318))
GLOBAL_UNIT_ASSIGNED_CONTEXT((#7345,#7347,#7348))
REPRESENTATION_CONTEXT('','3D')
);
#7345=(
LENGTH_UNIT()
NAMED_UNIT(*)
SI_UNIT(.CENTI.,.METRE.)
);
#7347=(
NAMED_UNIT(*)
PLANE_ANGLE_UNIT()
SI_UNIT($,.RADIAN.)
);
#7348=(
NAMED_UNIT(*)
SI_UNIT($,.STERADIAN.)
SOLID_ANGLE_UNIT()
);
#7360=SHAPE_DEFINITION_REPRESENTATION(#7385,#7451);
#7385=PRODUCT_DEFINITION_SHAPE('',$,#7477);
#7451=SHAPE_REPRESENTATION('',(#4620),#7330);
#7465=PRODUCT_DEFINITION_CONTEXT('part definition',#7542,'design');
#7477=PRODUCT_DEFINITION('Cap Screw - M6x25','Cap Screw - M6x25',#7502,
#7465);
#7502=PRODUCT_DEFINITION_FORMATION('',$,#7555);
#7542=APPLICATION_CONTEXT(
'Core Data for Automotive Mechanical Design Process');
#7543=PRODUCT_CONTEXT('part definition',#7542,'mechanical');
#7555=PRODUCT('Cap Screw - M6x25','Cap Screw - M6x25',
'Cap Screw - M6x25',(#7543));
#7632=COLOUR_RGB('Black',0.12,0.14,0.17);
#7633=FILL_AREA_STYLE_COLOUR('',#7632);
#7634=FILL_AREA_STYLE('',(#7633));
#7635=SURFACE_STYLE_FILL_AREA(#7634);
#7636=SURFACE_SIDE_STYLE('',(#7635));
#7637=SURFACE_STYLE_USAGE(.BOTH.,#7636);
#7638=PRESENTATION_STYLE_ASSIGNMENT((#7637));
ENDSEC;
END-ISO-10303-21;
